ISO-10303-21;
HEADER;
/* Generated by software containing ST-Developer
 * from STEP Tools, Inc. (www.steptools.com) 
 */

FILE_DESCRIPTION(
/* description */ ('STEP AP214'),
/* implementation_level */ '2;1');

FILE_NAME(
/* name */ 'Hex Nut M10 x 1.5.step',
/* time_stamp */ '2026-11-14T06:43:04-08:00',
/* author */ (''),
/* organization */ (''),
/* preprocessor_version */ 'ST-DEVELOPER v20.2',
/* originating_system */ 'Autodesk Translation Framework v15.17.0.0',
/* authorisation */ '');

FILE_SCHEMA (('AUTOMOTIVE_DESIGN { 1 0 10303 214 3 1 1 }'));
ENDSEC;

DATA;
#10=MECHANICAL_DESIGN_GEOMETRIC_PRESENTATION_REPRESENTATION('',(#203),#5658);
#95=CONICAL_SURFACE('',#3385,8.,1.0471975511966);
#96=CONICAL_SURFACE('',#3386,8.,1.0471975511966);
#97=CONICAL_SURFACE('',#3387,8.,1.0471975511966);
#98=CONICAL_SURFACE('',#3388,8.,1.0471975511966);
#99=CONICAL_SURFACE('',#3389,8.,1.0471975511966);
#100=CONICAL_SURFACE('',#3390,8.,1.0471975511966);
#101=CONICAL_SURFACE('',#3391,8.,1.0471975511966);
#102=CONICAL_SURFACE('',#3392,8.,1.0471975511966);
#103=CONICAL_SURFACE('',#3393,8.,1.0471975511966);
#104=CONICAL_SURFACE('',#3394,8.,1.0471975511966);
#105=CONICAL_SURFACE('',#3395,8.,1.0471975511966);
#106=CONICAL_SURFACE('',#3396,8.,1.0471975511966);
#141=(
BOUNDED_CURVE()
B_SPLINE_CURVE(2,(#5139,#5140,#5141),.UNSPECIFIED.,.F.,.F.)
B_SPLINE_CURVE_WITH_KNOTS((3,3),(1.54292191464265,2.47778215640189),
 .UNSPECIFIED.)
CURVE()
GEOMETRIC_REPRESENTATION_ITEM()
RATIONAL_B_SPLINE_CURVE((1.8727241335928,2.01757984944671,2.01757984944671))
REPRESENTATION_ITEM('')
);
#142=(
BOUNDED_CURVE()
B_SPLINE_CURVE(2,(#5143,#5144,#5145),.UNSPECIFIED.,.F.,.F.)
B_SPLINE_CURVE_WITH_KNOTS((3,3),(2.47778215640189,3.41264239816114),
 .UNSPECIFIED.)
CURVE()
GEOMETRIC_REPRESENTATION_ITEM()
RATIONAL_B_SPLINE_CURVE((2.01757984944671,2.01757984944671,1.8727241335928))
REPRESENTATION_ITEM('')
);
#143=(
BOUNDED_CURVE()
B_SPLINE_CURVE(2,(#5149,#5150,#5151),.UNSPECIFIED.,.F.,.F.)
B_SPLINE_CURVE_WITH_KNOTS((3,3),(-2.47778215640189,-1.54292191464263),
 .UNSPECIFIED.)
CURVE()
GEOMETRIC_REPRESENTATION_ITEM()
RATIONAL_B_SPLINE_CURVE((2.01757984944672,2.01757984944672,1.8727241335928))
REPRESENTATION_ITEM('')
);
#144=(
BOUNDED_CURVE()
B_SPLINE_CURVE(2,(#5152,#5153,#5154),.UNSPECIFIED.,.F.,.F.)
B_SPLINE_CURVE_WITH_KNOTS((3,3),(-3.41264239816113,-2.47778215640189),
 .UNSPECIFIED.)
CURVE()
GEOMETRIC_REPRESENTATION_ITEM()
RATIONAL_B_SPLINE_CURVE((1.8727241335928,2.01757984944671,2.01757984944671))
REPRESENTATION_ITEM('')
);
#145=(
BOUNDED_CURVE()
B_SPLINE_CURVE(2,(#5157,#5158,#5159),.UNSPECIFIED.,.F.,.F.)
B_SPLINE_CURVE_WITH_KNOTS((3,3),(1.54292191464264,2.47778215640189),
 .UNSPECIFIED.)
CURVE()
GEOMETRIC_REPRESENTATION_ITEM()
RATIONAL_B_SPLINE_CURVE((1.8727241335928,2.01757984944672,2.01757984944672))
REPRESENTATION_ITEM('')
);
#146=(
BOUNDED_CURVE()
B_SPLINE_CURVE(2,(#5161,#5162,#5163),.UNSPECIFIED.,.F.,.F.)
B_SPLINE_CURVE_WITH_KNOTS((3,3),(2.47778215640189,3.41264239816113),
 .UNSPECIFIED.)
CURVE()
GEOMETRIC_REPRESENTATION_ITEM()
RATIONAL_B_SPLINE_CURVE((2.01757984944672,2.01757984944672,1.87272413359281))
REPRESENTATION_ITEM('')
);
#147=(
BOUNDED_CURVE()
B_SPLINE_CURVE(2,(#5167,#5168,#5169),.UNSPECIFIED.,.F.,.F.)
B_SPLINE_CURVE_WITH_KNOTS((3,3),(-2.47778215640188,-1.54292191464265),
 .UNSPECIFIED.)
CURVE()
GEOMETRIC_REPRESENTATION_ITEM()
RATIONAL_B_SPLINE_CURVE((2.01757984944672,2.01757984944672,1.87272413359281))
REPRESENTATION_ITEM('')
);
#148=(
BOUNDED_CURVE()
B_SPLINE_CURVE(2,(#5170,#5171,#5172),.UNSPECIFIED.,.F.,.F.)
B_SPLINE_CURVE_WITH_KNOTS((3,3),(-3.41264239816114,-2.47778215640188),
 .UNSPECIFIED.)
CURVE()
GEOMETRIC_REPRESENTATION_ITEM()
RATIONAL_B_SPLINE_CURVE((1.8727241335928,2.01757984944672,2.01757984944672))
REPRESENTATION_ITEM('')
);
#149=(
BOUNDED_CURVE()
B_SPLINE_CURVE(2,(#5176,#5177,#5178),.UNSPECIFIED.,.F.,.F.)
B_SPLINE_CURVE_WITH_KNOTS((3,3),(1.54292191464263,2.47778215640189),
 .UNSPECIFIED.)
CURVE()
GEOMETRIC_REPRESENTATION_ITEM()
RATIONAL_B_SPLINE_CURVE((1.8727241335928,2.01757984944671,2.01757984944671))
REPRESENTATION_ITEM('')
);
#150=(
BOUNDED_CURVE()
B_SPLINE_CURVE(2,(#5182,#5183,#5184),.UNSPECIFIED.,.F.,.F.)
B_SPLINE_CURVE_WITH_KNOTS((3,3),(-3.41264239816114,-2.47778215640189),
 .UNSPECIFIED.)
CURVE()
GEOMETRIC_REPRESENTATION_ITEM()
RATIONAL_B_SPLINE_CURVE((1.8727241335928,2.01757984944671,2.01757984944671))
REPRESENTATION_ITEM('')
);
#151=(
BOUNDED_CURVE()
B_SPLINE_CURVE(2,(#5185,#5186,#5187),.UNSPECIFIED.,.F.,.F.)
B_SPLINE_CURVE_WITH_KNOTS((3,3),(-2.47778215640189,-1.54292191464264),
 .UNSPECIFIED.)
CURVE()
GEOMETRIC_REPRESENTATION_ITEM()
RATIONAL_B_SPLINE_CURVE((2.01757984944671,2.01757984944672,1.8727241335928))
REPRESENTATION_ITEM('')
);
#152=(
BOUNDED_CURVE()
B_SPLINE_CURVE(2,(#5188,#5189,#5190),.UNSPECIFIED.,.F.,.F.)
B_SPLINE_CURVE_WITH_KNOTS((3,3),(2.47778215640189,3.41264239816114),
 .UNSPECIFIED.)
CURVE()
GEOMETRIC_REPRESENTATION_ITEM()
RATIONAL_B_SPLINE_CURVE((2.01757984944671,2.01757984944672,1.8727241335928))
REPRESENTATION_ITEM('')
);
#153=(
BOUNDED_CURVE()
B_SPLINE_CURVE(2,(#5193,#5194,#5195),.UNSPECIFIED.,.F.,.F.)
B_SPLINE_CURVE_WITH_KNOTS((3,3),(1.54292191464265,2.47778215640188),
 .UNSPECIFIED.)
CURVE()
GEOMETRIC_REPRESENTATION_ITEM()
RATIONAL_B_SPLINE_CURVE((1.8727241335928,2.01757984944671,2.01757984944671))
REPRESENTATION_ITEM('')
);
#154=(
BOUNDED_CURVE()
B_SPLINE_CURVE(2,(#5197,#5198,#5199),.UNSPECIFIED.,.F.,.F.)
B_SPLINE_CURVE_WITH_KNOTS((3,3),(2.47778215640188,3.41264239816114),
 .UNSPECIFIED.)
CURVE()
GEOMETRIC_REPRESENTATION_ITEM()
RATIONAL_B_SPLINE_CURVE((2.01757984944671,2.01757984944671,1.87272413359279))
REPRESENTATION_ITEM('')
);
#155=(
BOUNDED_CURVE()
B_SPLINE_CURVE(2,(#5203,#5204,#5205),.UNSPECIFIED.,.F.,.F.)
B_SPLINE_CURVE_WITH_KNOTS((3,3),(-2.47778215640188,-1.54292191464263),
 .UNSPECIFIED.)
CURVE()
GEOMETRIC_REPRESENTATION_ITEM()
RATIONAL_B_SPLINE_CURVE((2.01757984944671,2.01757984944671,1.87272413359279))
REPRESENTATION_ITEM('')
);
#156=(
BOUNDED_CURVE()
B_SPLINE_CURVE(2,(#5206,#5207,#5208),.UNSPECIFIED.,.F.,.F.)
B_SPLINE_CURVE_WITH_KNOTS((3,3),(-3.41264239816112,-2.47778215640188),
 .UNSPECIFIED.)
CURVE()
GEOMETRIC_REPRESENTATION_ITEM()
RATIONAL_B_SPLINE_CURVE((1.8727241335928,2.01757984944671,2.01757984944671))
REPRESENTATION_ITEM('')
);
#157=(
BOUNDED_CURVE()
B_SPLINE_CURVE(2,(#5211,#5212,#5213),.UNSPECIFIED.,.F.,.F.)
B_SPLINE_CURVE_WITH_KNOTS((3,3),(1.54292191464265,2.47778215640188),
 .UNSPECIFIED.)
CURVE()
GEOMETRIC_REPRESENTATION_ITEM()
RATIONAL_B_SPLINE_CURVE((1.8727241335928,2.01757984944671,2.01757984944671))
REPRESENTATION_ITEM('')
);
#158=(
BOUNDED_CURVE()
B_SPLINE_CURVE(2,(#5215,#5216,#5217),.UNSPECIFIED.,.F.,.F.)
B_SPLINE_CURVE_WITH_KNOTS((3,3),(2.47778215640188,3.41264239816112),
 .UNSPECIFIED.)
CURVE()
GEOMETRIC_REPRESENTATION_ITEM()
RATIONAL_B_SPLINE_CURVE((2.01757984944671,2.01757984944671,1.8727241335928))
REPRESENTATION_ITEM('')
);
#159=(
BOUNDED_CURVE()
B_SPLINE_CURVE(2,(#5221,#5222,#5223),.UNSPECIFIED.,.F.,.F.)
B_SPLINE_CURVE_WITH_KNOTS((3,3),(-2.47778215640189,-1.54292191464265),
 .UNSPECIFIED.)
CURVE()
GEOMETRIC_REPRESENTATION_ITEM()
RATIONAL_B_SPLINE_CURVE((2.0175798494467,2.01757984944671,1.8727241335928))
REPRESENTATION_ITEM('')
);
#160=(
BOUNDED_CURVE()
B_SPLINE_CURVE(2,(#5224,#5225,#5226),.UNSPECIFIED.,.F.,.F.)
B_SPLINE_CURVE_WITH_KNOTS((3,3),(-3.41264239816112,-2.47778215640189),
 .UNSPECIFIED.)
CURVE()
GEOMETRIC_REPRESENTATION_ITEM()
RATIONAL_B_SPLINE_CURVE((1.8727241335928,2.0175798494467,2.0175798494467))
REPRESENTATION_ITEM('')
);
#161=(
BOUNDED_CURVE()
B_SPLINE_CURVE(2,(#5229,#5230,#5231),.UNSPECIFIED.,.F.,.F.)
B_SPLINE_CURVE_WITH_KNOTS((3,3),(1.54292191464263,2.47778215640189),
 .UNSPECIFIED.)
CURVE()
GEOMETRIC_REPRESENTATION_ITEM()
RATIONAL_B_SPLINE_CURVE((1.8727241335928,2.01757984944671,2.01757984944671))
REPRESENTATION_ITEM('')
);
#162=(
BOUNDED_CURVE()
B_SPLINE_CURVE(2,(#5232,#5233,#5234),.UNSPECIFIED.,.F.,.F.)
B_SPLINE_CURVE_WITH_KNOTS((3,3),(2.47778215640189,3.41264239816113),
 .UNSPECIFIED.)
CURVE()
GEOMETRIC_REPRESENTATION_ITEM()
RATIONAL_B_SPLINE_CURVE((2.01757984944671,2.01757984944671,1.8727241335928))
REPRESENTATION_ITEM('')
);
#163=(
BOUNDED_CURVE()
B_SPLINE_CURVE(2,(#5236,#5237,#5238),.UNSPECIFIED.,.F.,.F.)
B_SPLINE_CURVE_WITH_KNOTS((3,3),(-2.47778215640189,-1.54292191464264),
 .UNSPECIFIED.)
CURVE()
GEOMETRIC_REPRESENTATION_ITEM()
RATIONAL_B_SPLINE_CURVE((2.01757984944671,2.01757984944672,1.8727241335928))
REPRESENTATION_ITEM('')
);
#164=(
BOUNDED_CURVE()
B_SPLINE_CURVE(2,(#5239,#5240,#5241),.UNSPECIFIED.,.F.,.F.)
B_SPLINE_CURVE_WITH_KNOTS((3,3),(-3.41264239816114,-2.47778215640189),
 .UNSPECIFIED.)
CURVE()
GEOMETRIC_REPRESENTATION_ITEM()
RATIONAL_B_SPLINE_CURVE((1.8727241335928,2.01757984944671,2.01757984944671))
REPRESENTATION_ITEM('')
);
#181=SHAPE_REPRESENTATION_RELATIONSHIP('SRR','None',#5711,#192);
#192=ADVANCED_BREP_SHAPE_REPRESENTATION('',(#214),#5652);
#203=STYLED_ITEM('',(#5770),#214);
#214=MANIFOLD_SOLID_BREP('Body1',#3065);
#253=CYLINDRICAL_SURFACE('',#3362,5.);
#309=FACE_BOUND('',#651,.T.);
#310=FACE_BOUND('',#653,.T.);
#423=FACE_OUTER_BOUND('',#643,.T.);
#424=FACE_OUTER_BOUND('',#644,.T.);
#425=FACE_OUTER_BOUND('',#645,.T.);
#426=FACE_OUTER_BOUND('',#646,.T.);
#427=FACE_OUTER_BOUND('',#647,.T.);
#428=FACE_OUTER_BOUND('',#648,.T.);
#429=FACE_OUTER_BOUND('',#649,.T.);
#430=FACE_OUTER_BOUND('',#650,.T.);
#431=FACE_OUTER_BOUND('',#652,.T.);
#432=FACE_OUTER_BOUND('',#654,.T.);
#433=FACE_OUTER_BOUND('',#655,.T.);
#434=FACE_OUTER_BOUND('',#656,.T.);
#435=FACE_OUTER_BOUND('',#657,.T.);
#436=FACE_OUTER_BOUND('',#658,.T.);
#437=FACE_OUTER_BOUND('',#659,.T.);
#438=FACE_OUTER_BOUND('',#660,.T.);
#439=FACE_OUTER_BOUND('',#661,.T.);
#440=FACE_OUTER_BOUND('',#662,.T.);
#441=FACE_OUTER_BOUND('',#663,.T.);
#442=FACE_OUTER_BOUND('',#664,.T.);
#443=FACE_OUTER_BOUND('',#665,.T.);
#643=EDGE_LOOP('',(#2370,#2371,#2372,#2373));
#644=EDGE_LOOP('',(#2374,#2375,#2376,#2377,#2378,#2379));
#645=EDGE_LOOP('',(#2380,#2381,#2382,#2383,#2384,#2385));
#646=EDGE_LOOP('',(#2386,#2387,#2388,#2389,#2390,#2391));
#647=EDGE_LOOP('',(#2392,#2393,#2394,#2395,#2396,#2397));
#648=EDGE_LOOP('',(#2398,#2399,#2400,#2401,#2402,#2403));
#649=EDGE_LOOP('',(#2404,#2405,#2406,#2407,#2408,#2409));
#650=EDGE_LOOP('',(#2410,#2411,#2412,#2413,#2414,#2415));
#651=EDGE_LOOP('',(#2416));
#652=EDGE_LOOP('',(#2417,#2418,#2419,#2420,#2421,#2422));
#653=EDGE_LOOP('',(#2423));
#654=EDGE_LOOP('',(#2424,#2425,#2426));
#655=EDGE_LOOP('',(#2427,#2428,#2429));
#656=EDGE_LOOP('',(#2430,#2431,#2432));
#657=EDGE_LOOP('',(#2433,#2434,#2435));
#658=EDGE_LOOP('',(#2436,#2437,#2438));
#659=EDGE_LOOP('',(#2439,#2440,#2441));
#660=EDGE_LOOP('',(#2442,#2443,#2444));
#661=EDGE_LOOP('',(#2445,#2446,#2447));
#662=EDGE_LOOP('',(#2448,#2449,#2450));
#663=EDGE_LOOP('',(#2451,#2452,#2453));
#664=EDGE_LOOP('',(#2454,#2455,#2456));
#665=EDGE_LOOP('',(#2457,#2458,#2459));
#857=LINE('',#5132,#1053);
#858=LINE('',#5137,#1054);
#859=LINE('',#5147,#1055);
#860=LINE('',#5165,#1056);
#861=LINE('',#5180,#1057);
#862=LINE('',#5201,#1058);
#863=LINE('',#5219,#1059);
#1053=VECTOR('',#3991,5.);
#1054=VECTOR('',#3996,1000.);
#1055=VECTOR('',#3997,1000.);
#1056=VECTOR('',#4000,1000.);
#1057=VECTOR('',#4003,1000.);
#1058=VECTOR('',#4006,1000.);
#1059=VECTOR('',#4009,1000.);
#1236=CIRCLE('',#3363,5.);
#1237=CIRCLE('',#3364,4.99999999999999);
#1238=CIRCLE('',#3372,8.);
#1239=CIRCLE('',#3373,8.);
#1240=CIRCLE('',#3374,8.);
#1241=CIRCLE('',#3375,8.);
#1242=CIRCLE('',#3376,8.);
#1243=CIRCLE('',#3377,8.);
#1244=CIRCLE('',#3379,8.);
#1245=CIRCLE('',#3380,8.);
#1246=CIRCLE('',#3381,8.);
#1247=CIRCLE('',#3382,8.);
#1248=CIRCLE('',#3383,8.);
#1249=CIRCLE('',#3384,8.);
#1441=VERTEX_POINT('',#5129);
#1442=VERTEX_POINT('',#5131);
#1443=VERTEX_POINT('',#5135);
#1444=VERTEX_POINT('',#5136);
#1445=VERTEX_POINT('',#5138);
#1446=VERTEX_POINT('',#5142);
#1447=VERTEX_POINT('',#5146);
#1448=VERTEX_POINT('',#5148);
#1449=VERTEX_POINT('',#5156);
#1450=VERTEX_POINT('',#5160);
#1451=VERTEX_POINT('',#5164);
#1452=VERTEX_POINT('',#5166);
#1453=VERTEX_POINT('',#5174);
#1454=VERTEX_POINT('',#5175);
#1455=VERTEX_POINT('',#5179);
#1456=VERTEX_POINT('',#5181);
#1457=VERTEX_POINT('',#5192);
#1458=VERTEX_POINT('',#5196);
#1459=VERTEX_POINT('',#5200);
#1460=VERTEX_POINT('',#5202);
#1461=VERTEX_POINT('',#5210);
#1462=VERTEX_POINT('',#5214);
#1463=VERTEX_POINT('',#5218);
#1464=VERTEX_POINT('',#5220);
#1465=VERTEX_POINT('',#5228);
#1466=VERTEX_POINT('',#5235);
#1768=EDGE_CURVE('',#1441,#1441,#1236,.T.);
#1769=EDGE_CURVE('',#1441,#1442,#857,.T.);
#1770=EDGE_CURVE('',#1442,#1442,#1237,.T.);
#1771=EDGE_CURVE('',#1443,#1444,#858,.T.);
#1772=EDGE_CURVE('',#1444,#1445,#141,.T.);
#1773=EDGE_CURVE('',#1445,#1446,#142,.T.);
#1774=EDGE_CURVE('',#1447,#1446,#859,.T.);
#1775=EDGE_CURVE('',#1448,#1447,#143,.T.);
#1776=EDGE_CURVE('',#1443,#1448,#144,.T.);
#1777=EDGE_CURVE('',#1446,#1449,#145,.T.);
#1778=EDGE_CURVE('',#1449,#1450,#146,.T.);
#1779=EDGE_CURVE('',#1451,#1450,#860,.T.);
#1780=EDGE_CURVE('',#1452,#1451,#147,.T.);
#1781=EDGE_CURVE('',#1447,#1452,#148,.T.);
#1782=EDGE_CURVE('',#1453,#1454,#149,.T.);
#1783=EDGE_CURVE('',#1455,#1453,#861,.T.);
#1784=EDGE_CURVE('',#1455,#1456,#150,.T.);
#1785=EDGE_CURVE('',#1456,#1451,#151,.T.);
#1786=EDGE_CURVE('',#1454,#1450,#152,.T.);
#1787=EDGE_CURVE('',#1453,#1457,#153,.T.);
#1788=EDGE_CURVE('',#1457,#1458,#154,.T.);
#1789=EDGE_CURVE('',#1459,#1458,#862,.T.);
#1790=EDGE_CURVE('',#1460,#1459,#155,.T.);
#1791=EDGE_CURVE('',#1455,#1460,#156,.T.);
#1792=EDGE_CURVE('',#1458,#1461,#157,.T.);
#1793=EDGE_CURVE('',#1461,#1462,#158,.T.);
#1794=EDGE_CURVE('',#1463,#1462,#863,.T.);
#1795=EDGE_CURVE('',#1464,#1463,#159,.T.);
#1796=EDGE_CURVE('',#1459,#1464,#160,.T.);
#1797=EDGE_CURVE('',#1462,#1465,#161,.T.);
#1798=EDGE_CURVE('',#1465,#1444,#162,.T.);
#1799=EDGE_CURVE('',#1466,#1443,#163,.T.);
#1800=EDGE_CURVE('',#1463,#1466,#164,.T.);
#1801=EDGE_CURVE('',#1465,#1445,#1238,.T.);
#1802=EDGE_CURVE('',#1461,#1465,#1239,.T.);
#1803=EDGE_CURVE('',#1457,#1461,#1240,.T.);
#1804=EDGE_CURVE('',#1454,#1457,#1241,.T.);
#1805=EDGE_CURVE('',#1454,#1449,#1242,.T.);
#1806=EDGE_CURVE('',#1445,#1449,#1243,.T.);
#1807=EDGE_CURVE('',#1466,#1464,#1244,.T.);
#1808=EDGE_CURVE('',#1448,#1466,#1245,.T.);
#1809=EDGE_CURVE('',#1452,#1448,#1246,.T.);
#1810=EDGE_CURVE('',#1456,#1452,#1247,.T.);
#1811=EDGE_CURVE('',#1460,#1456,#1248,.T.);
#1812=EDGE_CURVE('',#1464,#1460,#1249,.T.);
#2370=ORIENTED_EDGE('',*,*,#1768,.F.);
#2371=ORIENTED_EDGE('',*,*,#1769,.T.);
#2372=ORIENTED_EDGE('',*,*,#1770,.T.);
#2373=ORIENTED_EDGE('',*,*,#1769,.F.);
#2374=ORIENTED_EDGE('',*,*,#1771,.T.);
#2375=ORIENTED_EDGE('',*,*,#1772,.T.);
#2376=ORIENTED_EDGE('',*,*,#1773,.T.);
#2377=ORIENTED_EDGE('',*,*,#1774,.F.);
#2378=ORIENTED_EDGE('',*,*,#1775,.F.);
#2379=ORIENTED_EDGE('',*,*,#1776,.F.);
#2380=ORIENTED_EDGE('',*,*,#1774,.T.);
#2381=ORIENTED_EDGE('',*,*,#1777,.T.);
#2382=ORIENTED_EDGE('',*,*,#1778,.T.);
#2383=ORIENTED_EDGE('',*,*,#1779,.F.);
#2384=ORIENTED_EDGE('',*,*,#1780,.F.);
#2385=ORIENTED_EDGE('',*,*,#1781,.F.);
#2386=ORIENTED_EDGE('',*,*,#1782,.F.);
#2387=ORIENTED_EDGE('',*,*,#1783,.F.);
#2388=ORIENTED_EDGE('',*,*,#1784,.T.);
#2389=ORIENTED_EDGE('',*,*,#1785,.T.);
#2390=ORIENTED_EDGE('',*,*,#1779,.T.);
#2391=ORIENTED_EDGE('',*,*,#1786,.F.);
#2392=ORIENTED_EDGE('',*,*,#1783,.T.);
#2393=ORIENTED_EDGE('',*,*,#1787,.T.);
#2394=ORIENTED_EDGE('',*,*,#1788,.T.);
#2395=ORIENTED_EDGE('',*,*,#1789,.F.);
#2396=ORIENTED_EDGE('',*,*,#1790,.F.);
#2397=ORIENTED_EDGE('',*,*,#1791,.F.);
#2398=ORIENTED_EDGE('',*,*,#1789,.T.);
#2399=ORIENTED_EDGE('',*,*,#1792,.T.);
#2400=ORIENTED_EDGE('',*,*,#1793,.T.);
#2401=ORIENTED_EDGE('',*,*,#1794,.F.);
#2402=ORIENTED_EDGE('',*,*,#1795,.F.);
#2403=ORIENTED_EDGE('',*,*,#1796,.F.);
#2404=ORIENTED_EDGE('',*,*,#1794,.T.);
#2405=ORIENTED_EDGE('',*,*,#1797,.T.);
#2406=ORIENTED_EDGE('',*,*,#1798,.T.);
#2407=ORIENTED_EDGE('',*,*,#1771,.F.);
#2408=ORIENTED_EDGE('',*,*,#1799,.F.);
#2409=ORIENTED_EDGE('',*,*,#1800,.F.);
#2410=ORIENTED_EDGE('',*,*,#1801,.F.);
#2411=ORIENTED_EDGE('',*,*,#1802,.F.);
#2412=ORIENTED_EDGE('',*,*,#1803,.F.);
#2413=ORIENTED_EDGE('',*,*,#1804,.F.);
#2414=ORIENTED_EDGE('',*,*,#1805,.T.);
#2415=ORIENTED_EDGE('',*,*,#1806,.F.);
#2416=ORIENTED_EDGE('',*,*,#1770,.F.);
#2417=ORIENTED_EDGE('',*,*,#1807,.F.);
#2418=ORIENTED_EDGE('',*,*,#1808,.F.);
#2419=ORIENTED_EDGE('',*,*,#1809,.F.);
#2420=ORIENTED_EDGE('',*,*,#1810,.F.);
#2421=ORIENTED_EDGE('',*,*,#1811,.F.);
#2422=ORIENTED_EDGE('',*,*,#1812,.F.);
#2423=ORIENTED_EDGE('',*,*,#1768,.T.);
#2424=ORIENTED_EDGE('',*,*,#1776,.T.);
#2425=ORIENTED_EDGE('',*,*,#1808,.T.);
#2426=ORIENTED_EDGE('',*,*,#1799,.T.);
#2427=ORIENTED_EDGE('',*,*,#1775,.T.);
#2428=ORIENTED_EDGE('',*,*,#1781,.T.);
#2429=ORIENTED_EDGE('',*,*,#1809,.T.);
#2430=ORIENTED_EDGE('',*,*,#1780,.T.);
#2431=ORIENTED_EDGE('',*,*,#1785,.F.);
#2432=ORIENTED_EDGE('',*,*,#1810,.T.);
#2433=ORIENTED_EDGE('',*,*,#1791,.T.);
#2434=ORIENTED_EDGE('',*,*,#1811,.T.);
#2435=ORIENTED_EDGE('',*,*,#1784,.F.);
#2436=ORIENTED_EDGE('',*,*,#1790,.T.);
#2437=ORIENTED_EDGE('',*,*,#1796,.T.);
#2438=ORIENTED_EDGE('',*,*,#1812,.T.);
#2439=ORIENTED_EDGE('',*,*,#1795,.T.);
#2440=ORIENTED_EDGE('',*,*,#1800,.T.);
#2441=ORIENTED_EDGE('',*,*,#1807,.T.);
#2442=ORIENTED_EDGE('',*,*,#1802,.T.);
#2443=ORIENTED_EDGE('',*,*,#1797,.F.);
#2444=ORIENTED_EDGE('',*,*,#1793,.F.);
#2445=ORIENTED_EDGE('',*,*,#1803,.T.);
#2446=ORIENTED_EDGE('',*,*,#1792,.F.);
#2447=ORIENTED_EDGE('',*,*,#1788,.F.);
#2448=ORIENTED_EDGE('',*,*,#1782,.T.);
#2449=ORIENTED_EDGE('',*,*,#1804,.T.);
#2450=ORIENTED_EDGE('',*,*,#1787,.F.);
#2451=ORIENTED_EDGE('',*,*,#1805,.F.);
#2452=ORIENTED_EDGE('',*,*,#1786,.T.);
#2453=ORIENTED_EDGE('',*,*,#1778,.F.);
#2454=ORIENTED_EDGE('',*,*,#1806,.T.);
#2455=ORIENTED_EDGE('',*,*,#1777,.F.);
#2456=ORIENTED_EDGE('',*,*,#1773,.F.);
#2457=ORIENTED_EDGE('',*,*,#1798,.F.);
#2458=ORIENTED_EDGE('',*,*,#1801,.T.);
#2459=ORIENTED_EDGE('',*,*,#1772,.F.);
#2824=PLANE('',#3365);
#2825=PLANE('',#3366);
#2826=PLANE('',#3367);
#2827=PLANE('',#3368);
#2828=PLANE('',#3369);
#2829=PLANE('',#3370);
#2830=PLANE('',#3371);
#2831=PLANE('',#3378);
#2964=ADVANCED_FACE('',(#423),#253,.F.);
#2965=ADVANCED_FACE('',(#424),#2824,.T.);
#2966=ADVANCED_FACE('',(#425),#2825,.T.);
#2967=ADVANCED_FACE('',(#426),#2826,.F.);
#2968=ADVANCED_FACE('',(#427),#2827,.T.);
#2969=ADVANCED_FACE('',(#428),#2828,.T.);
#2970=ADVANCED_FACE('',(#429),#2829,.T.);
#2971=ADVANCED_FACE('',(#430,#309),#2830,.F.);
#2972=ADVANCED_FACE('',(#431,#310),#2831,.T.);
#2973=ADVANCED_FACE('',(#432),#95,.T.);
#2974=ADVANCED_FACE('',(#433),#96,.T.);
#2975=ADVANCED_FACE('',(#434),#97,.T.);
#2976=ADVANCED_FACE('',(#435),#98,.T.);
#2977=ADVANCED_FACE('',(#436),#99,.T.);
#2978=ADVANCED_FACE('',(#437),#100,.T.);
#2979=ADVANCED_FACE('',(#438),#101,.T.);
#2980=ADVANCED_FACE('',(#439),#102,.T.);
#2981=ADVANCED_FACE('',(#440),#103,.T.);
#2982=ADVANCED_FACE('',(#441),#104,.T.);
#2983=ADVANCED_FACE('',(#442),#105,.T.);
#2984=ADVANCED_FACE('',(#443),#106,.T.);
#3065=CLOSED_SHELL('',(#2964,#2965,#2966,#2967,#2968,#2969,#2970,#2971,
#2972,#2973,#2974,#2975,#2976,#2977,#2978,#2979,#2980,#2981,#2982,#2983,
#2984));
#3361=AXIS2_PLACEMENT_3D('',#5127,#3985,#3986);
#3362=AXIS2_PLACEMENT_3D('',#5128,#3987,#3988);
#3363=AXIS2_PLACEMENT_3D('',#5130,#3989,#3990);
#3364=AXIS2_PLACEMENT_3D('',#5133,#3992,#3993);
#3365=AXIS2_PLACEMENT_3D('',#5134,#3994,#3995);
#3366=AXIS2_PLACEMENT_3D('',#5155,#3998,#3999);
#3367=AXIS2_PLACEMENT_3D('',#5173,#4001,#4002);
#3368=AXIS2_PLACEMENT_3D('',#5191,#4004,#4005);
#3369=AXIS2_PLACEMENT_3D('',#5209,#4007,#4008);
#3370=AXIS2_PLACEMENT_3D('',#5227,#4010,#4011);
#3371=AXIS2_PLACEMENT_3D('',#5242,#4012,#4013);
#3372=AXIS2_PLACEMENT_3D('',#5243,#4014,#4015);
#3373=AXIS2_PLACEMENT_3D('',#5244,#4016,#4017);
#3374=AXIS2_PLACEMENT_3D('',#5245,#4018,#4019);
#3375=AXIS2_PLACEMENT_3D('',#5246,#4020,#4021);
#3376=AXIS2_PLACEMENT_3D('',#5247,#4022,#4023);
#3377=AXIS2_PLACEMENT_3D('',#5248,#4024,#4025);
#3378=AXIS2_PLACEMENT_3D('',#5249,#4026,#4027);
#3379=AXIS2_PLACEMENT_3D('',#5250,#4028,#4029);
#3380=AXIS2_PLACEMENT_3D('',#5251,#4030,#4031);
#3381=AXIS2_PLACEMENT_3D('',#5252,#4032,#4033);
#3382=AXIS2_PLACEMENT_3D('',#5253,#4034,#4035);
#3383=AXIS2_PLACEMENT_3D('',#5254,#4036,#4037);
#3384=AXIS2_PLACEMENT_3D('',#5255,#4038,#4039);
#3385=AXIS2_PLACEMENT_3D('',#5256,#4040,#4041);
#3386=AXIS2_PLACEMENT_3D('',#5257,#4042,#4043);
#3387=AXIS2_PLACEMENT_3D('',#5258,#4044,#4045);
#3388=AXIS2_PLACEMENT_3D('',#5259,#4046,#4047);
#3389=AXIS2_PLACEMENT_3D('',#5260,#4048,#4049);
#3390=AXIS2_PLACEMENT_3D('',#5261,#4050,#4051);
#3391=AXIS2_PLACEMENT_3D('',#5262,#4052,#4053);
#3392=AXIS2_PLACEMENT_3D('',#5263,#4054,#4055);
#3393=AXIS2_PLACEMENT_3D('',#5264,#4056,#4057);
#3394=AXIS2_PLACEMENT_3D('',#5265,#4058,#4059);
#3395=AXIS2_PLACEMENT_3D('',#5266,#4060,#4061);
#3396=AXIS2_PLACEMENT_3D('',#5267,#4062,#4063);
#3985=DIRECTION('axis',(0.,0.,1.));
#3986=DIRECTION('refdir',(1.,0.,0.));
#3987=DIRECTION('center_axis',(0.,0.,1.));
#3988=DIRECTION('ref_axis',(1.,0.,0.));
#3989=DIRECTION('center_axis',(0.,0.,1.));
#3990=DIRECTION('ref_axis',(-1.,0.,0.));
#3991=DIRECTION('',(0.,0.,1.));
#3992=DIRECTION('center_axis',(0.,0.,1.));
#3993=DIRECTION('ref_axis',(1.,0.,0.));
#3994=DIRECTION('center_axis',(-0.500000000000003,0.866025403784437,0.));
#3995=DIRECTION('ref_axis',(-0.866025403784437,-0.500000000000003,0.));
#3996=DIRECTION('',(0.,0.,1.));
#3997=DIRECTION('',(0.,0.,1.));
#3998=DIRECTION('center_axis',(0.500000000000004,0.866025403784437,0.));
#3999=DIRECTION('ref_axis',(-0.866025403784437,0.500000000000004,0.));
#4000=DIRECTION('',(0.,0.,1.));
#4001=DIRECTION('center_axis',(-1.,0.,0.));
#4002=DIRECTION('ref_axis',(0.,0.,1.));
#4003=DIRECTION('',(0.,0.,1.));
#4004=DIRECTION('center_axis',(0.500000000000002,-0.866025403784437,0.));
#4005=DIRECTION('ref_axis',(0.866025403784437,0.500000000000002,0.));
#4006=DIRECTION('',(0.,0.,1.));
#4007=DIRECTION('center_axis',(-0.500000000000003,-0.866025403784437,0.));
#4008=DIRECTION('ref_axis',(0.866025403784437,-0.500000000000003,0.));
#4009=DIRECTION('',(0.,0.,1.));
#4010=DIRECTION('center_axis',(-1.,0.,0.));
#4011=DIRECTION('ref_axis',(0.,0.,1.));
#4012=DIRECTION('center_axis',(0.,0.,-1.));
#4013=DIRECTION('ref_axis',(-1.,0.,0.));
#4014=DIRECTION('center_axis',(0.,0.,-1.));
#4015=DIRECTION('ref_axis',(-1.,0.,0.));
#4016=DIRECTION('center_axis',(0.,0.,-1.));
#4017=DIRECTION('ref_axis',(-1.,0.,0.));
#4018=DIRECTION('center_axis',(0.,0.,-1.));
#4019=DIRECTION('ref_axis',(-1.,0.,0.));
#4020=DIRECTION('center_axis',(0.,0.,-1.));
#4021=DIRECTION('ref_axis',(-1.,0.,0.));
#4022=DIRECTION('center_axis',(0.,0.,1.));
#4023=DIRECTION('ref_axis',(1.,0.,0.));
#4024=DIRECTION('center_axis',(0.,0.,-1.));
#4025=DIRECTION('ref_axis',(-1.,0.,0.));
#4026=DIRECTION('center_axis',(0.,0.,-1.));
#4027=DIRECTION('ref_axis',(-1.,0.,0.));
#4028=DIRECTION('center_axis',(0.,0.,1.));
#4029=DIRECTION('ref_axis',(-1.,0.,0.));
#4030=DIRECTION('center_axis',(0.,0.,1.));
#4031=DIRECTION('ref_axis',(-1.,-3.5527136788005E-15,0.));
#4032=DIRECTION('center_axis',(0.,0.,1.));
#4033=DIRECTION('ref_axis',(-1.,0.,0.));
#4034=DIRECTION('center_axis',(0.,0.,1.));
#4035=DIRECTION('ref_axis',(1.,0.,0.));
#4036=DIRECTION('center_axis',(0.,0.,1.));
#4037=DIRECTION('ref_axis',(-1.,1.77635683940025E-15,0.));
#4038=DIRECTION('center_axis',(0.,0.,1.));
#4039=DIRECTION('ref_axis',(-1.,0.,0.));
#4040=DIRECTION('center_axis',(0.,0.,1.));
#4041=DIRECTION('ref_axis',(1.,0.,0.));
#4042=DIRECTION('center_axis',(0.,0.,1.));
#4043=DIRECTION('ref_axis',(1.,0.,0.));
#4044=DIRECTION('center_axis',(0.,0.,1.));
#4045=DIRECTION('ref_axis',(1.,0.,0.));
#4046=DIRECTION('center_axis',(0.,0.,1.));
#4047=DIRECTION('ref_axis',(1.,0.,0.));
#4048=DIRECTION('center_axis',(0.,0.,1.));
#4049=DIRECTION('ref_axis',(1.,0.,0.));
#4050=DIRECTION('center_axis',(0.,0.,1.));
#4051=DIRECTION('ref_axis',(1.,0.,0.));
#4052=DIRECTION('center_axis',(0.,0.,-1.));
#4053=DIRECTION('ref_axis',(-1.,0.,0.));
#4054=DIRECTION('center_axis',(0.,0.,-1.));
#4055=DIRECTION('ref_axis',(-1.,0.,0.));
#4056=DIRECTION('center_axis',(0.,0.,-1.));
#4057=DIRECTION('ref_axis',(-1.,0.,0.));
#4058=DIRECTION('center_axis',(0.,0.,-1.));
#4059=DIRECTION('ref_axis',(-1.,0.,0.));
#4060=DIRECTION('center_axis',(0.,0.,-1.));
#4061=DIRECTION('ref_axis',(-1.,0.,0.));
#4062=DIRECTION('center_axis',(0.,0.,-1.));
#4063=DIRECTION('ref_axis',(-1.,0.,0.));
#5127=CARTESIAN_POINT('',(0.,0.,0.));
#5128=CARTESIAN_POINT('Origin',(0.,0.,-25.0375057290932));
#5129=CARTESIAN_POINT('',(-5.,-6.12323399573677E-16,-8.4));
#5130=CARTESIAN_POINT('Origin',(0.,0.,-8.4));
#5131=CARTESIAN_POINT('',(-5.,-6.12323399573677E-16,0.));
#5132=CARTESIAN_POINT('',(-5.,-6.12323399573677E-16,-25.0375057290932));
#5133=CARTESIAN_POINT('Origin',(0.,0.,3.25260651745651E-16));
#5134=CARTESIAN_POINT('Origin',(1.58955611655707E-15,9.23760430703403,-8.4));
#5135=CARTESIAN_POINT('',(-8.,4.61880215351705,-7.68546882018366));
#5136=CARTESIAN_POINT('',(-8.,4.61880215351699,-0.714531179816323));
#5137=CARTESIAN_POINT('',(-8.,4.61880215351699,-8.4));
#5138=CARTESIAN_POINT('',(-4.00000000000002,6.9282032302755,0.));
#5139=CARTESIAN_POINT('Ctrl Pts',(-8.00000000003847,4.61880215349478,-0.714531179829145));
#5140=CARTESIAN_POINT('Ctrl Pts',(-5.85640646056649,5.85640646054208,-8.88178419700125E-16));
#5141=CARTESIAN_POINT('Ctrl Pts',(-4.00000000000002,6.9282032302755,-8.80439423444571E-16));
#5142=CARTESIAN_POINT('',(-2.60208521396521E-15,9.23760430703403,-0.71453117981634));
#5143=CARTESIAN_POINT('Ctrl Pts',(-4.00000000000002,6.9282032302755,-8.80439423444571E-16));
#5144=CARTESIAN_POINT('Ctrl Pts',(-2.14359353943353,8.00000000000893,-8.83359324974957E-16));
#5145=CARTESIAN_POINT('Ctrl Pts',(3.84704779639695E-11,9.23760430705624,
-0.714531179829162));
#5146=CARTESIAN_POINT('',(8.67361737988404E-16,9.23760430703403,-7.68546882018366));
#5147=CARTESIAN_POINT('',(1.58955611655707E-15,9.23760430703403,-8.4));
#5148=CARTESIAN_POINT('',(-4.00000000000002,6.9282032302755,-8.4));
#5149=CARTESIAN_POINT('Ctrl Pts',(-4.00000000000004,6.92820323027549,-8.4));
#5150=CARTESIAN_POINT('Ctrl Pts',(-2.14359353943354,8.00000000000893,-8.4));
#5151=CARTESIAN_POINT('Ctrl Pts',(3.84766434846935E-11,9.23760430705625,
-7.68546882017083));
#5152=CARTESIAN_POINT('Ctrl Pts',(-8.00000000003847,4.61880215349478,-7.68546882017085));
#5153=CARTESIAN_POINT('Ctrl Pts',(-5.8564064605665,5.85640646054207,-8.4));
#5154=CARTESIAN_POINT('Ctrl Pts',(-4.00000000000004,6.92820323027549,-8.4));
#5155=CARTESIAN_POINT('Origin',(8.,4.61880215351698,-8.4));
#5156=CARTESIAN_POINT('',(4.00000000000003,6.92820323027549,0.));
#5157=CARTESIAN_POINT('Ctrl Pts',(-3.84662095265451E-11,9.23760430705625,
-0.714531179829163));
#5158=CARTESIAN_POINT('Ctrl Pts',(2.14359353943354,8.00000000000893,-6.66133814775094E-16));
#5159=CARTESIAN_POINT('Ctrl Pts',(4.00000000000003,6.9282032302755,-1.10054927930571E-15));
#5160=CARTESIAN_POINT('',(8.,4.61880215351705,-0.71453117981634));
#5161=CARTESIAN_POINT('Ctrl Pts',(4.00000000000003,6.9282032302755,-1.10054927930571E-15));
#5162=CARTESIAN_POINT('Ctrl Pts',(5.85640646056649,5.85640646054208,-1.85819040300646E-15));
#5163=CARTESIAN_POINT('Ctrl Pts',(8.00000000003845,4.61880215349479,-0.71453117982914));
#5164=CARTESIAN_POINT('',(8.,4.61880215351705,-7.68546882018366));
#5165=CARTESIAN_POINT('',(8.,4.61880215351698,-8.4));
#5166=CARTESIAN_POINT('',(4.00000000000003,6.92820323027549,-8.4));
#5167=CARTESIAN_POINT('Ctrl Pts',(4.00000000000004,6.92820323027549,-8.4));
#5168=CARTESIAN_POINT('Ctrl Pts',(5.85640646056649,5.85640646054208,-8.4));
#5169=CARTESIAN_POINT('Ctrl Pts',(8.00000000003844,4.61880215349479,-7.68546882017086));
#5170=CARTESIAN_POINT('Ctrl Pts',(-3.84676323390199E-11,9.23760430705624,
-7.68546882017084));
#5171=CARTESIAN_POINT('Ctrl Pts',(2.14359353943355,8.00000000000892,-8.4));
#5172=CARTESIAN_POINT('Ctrl Pts',(4.00000000000004,6.92820323027549,-8.4));
#5173=CARTESIAN_POINT('Origin',(8.,4.61880215351698,-8.4));
#5174=CARTESIAN_POINT('',(8.,-4.61880215351705,-0.71453117981634));
#5175=CARTESIAN_POINT('',(8.,0.,0.));
#5176=CARTESIAN_POINT('Ctrl Pts',(8.00000000000001,-4.61880215356147,-0.714531179829163));
#5177=CARTESIAN_POINT('Ctrl Pts',(8.00000000000001,-2.14359353946685,-3.88578058618805E-16));
#5178=CARTESIAN_POINT('Ctrl Pts',(8.,4.40219711722286E-15,-8.80439423444572E-16));
#5179=CARTESIAN_POINT('',(8.,-4.61880215351705,-7.68546882018366));
#5180=CARTESIAN_POINT('',(8.,-4.61880215351705,-8.4));
#5181=CARTESIAN_POINT('',(8.,0.,-8.4));
#5182=CARTESIAN_POINT('Ctrl Pts',(8.,-4.61880215356146,-7.68546882017084));
#5183=CARTESIAN_POINT('Ctrl Pts',(8.,-2.14359353946686,-8.4));
#5184=CARTESIAN_POINT('Ctrl Pts',(8.,-1.49674701985577E-14,-8.4));
#5185=CARTESIAN_POINT('Ctrl Pts',(8.,-1.49674701985577E-14,-8.4));
#5186=CARTESIAN_POINT('Ctrl Pts',(8.,2.14359353946684,-8.4));
#5187=CARTESIAN_POINT('Ctrl Pts',(8.,4.61880215356146,-7.68546882017084));
#5188=CARTESIAN_POINT('Ctrl Pts',(8.,-7.04351538755657E-15,4.40219711722283E-16));
#5189=CARTESIAN_POINT('Ctrl Pts',(8.,2.14359353946685,1.78210854566576E-15));
#5190=CARTESIAN_POINT('Ctrl Pts',(8.,4.61880215356148,-0.714531179829165));
#5191=CARTESIAN_POINT('Origin',(-3.00462919747434E-15,-9.23760430703408,
-8.4));
#5192=CARTESIAN_POINT('',(4.00000000000002,-6.9282032302755,0.));
#5193=CARTESIAN_POINT('Ctrl Pts',(8.00000000003846,-4.61880215349484,-0.714531179829161));
#5194=CARTESIAN_POINT('Ctrl Pts',(5.85640646056651,-5.85640646054213,-2.80331313717852E-14));
#5195=CARTESIAN_POINT('Ctrl Pts',(4.00000000000005,-6.92820323027554,-2.72936221267818E-14));
#5196=CARTESIAN_POINT('',(-8.93382590128056E-14,-9.23760430703403,-0.71453117981634));
#5197=CARTESIAN_POINT('Ctrl Pts',(4.00000000000005,-6.92820323027554,-2.72936221267818E-14));
#5198=CARTESIAN_POINT('Ctrl Pts',(2.14359353943354,-8.00000000000898,-2.65463710222373E-14));
#5199=CARTESIAN_POINT('Ctrl Pts',(-3.84861289011922E-11,-9.2376043070563,
-0.714531179829196));
#5200=CARTESIAN_POINT('',(-8.93382590128056E-14,-9.23760430703403,-7.68546882018366));
#5201=CARTESIAN_POINT('',(-3.00462919747434E-15,-9.23760430703408,-8.4));
#5202=CARTESIAN_POINT('',(4.00000000000002,-6.9282032302755,-8.4));
#5203=CARTESIAN_POINT('Ctrl Pts',(4.00000000000004,-6.92820323027554,-8.39999999999997));
#5204=CARTESIAN_POINT('Ctrl Pts',(2.14359353943353,-8.00000000000898,-8.39999999999997));
#5205=CARTESIAN_POINT('Ctrl Pts',(-3.85013055675899E-11,-9.23760430705631,
-7.6854688201708));
#5206=CARTESIAN_POINT('Ctrl Pts',(8.00000000003848,-4.61880215349483,-7.68546882017083));
#5207=CARTESIAN_POINT('Ctrl Pts',(5.85640646056651,-5.85640646054213,-8.39999999999997));
#5208=CARTESIAN_POINT('Ctrl Pts',(4.00000000000004,-6.92820323027554,-8.39999999999997));
#5209=CARTESIAN_POINT('Origin',(-8.,-4.61880215351704,-8.4));
#5210=CARTESIAN_POINT('',(-4.00000000000003,-6.92820323027549,0.));
#5211=CARTESIAN_POINT('Ctrl Pts',(3.83779951531087E-11,-9.23760430705625,
-0.714531179829162));
#5212=CARTESIAN_POINT('Ctrl Pts',(-2.14359353943358,-8.00000000000896,-2.75890421619351E-14));
#5213=CARTESIAN_POINT('Ctrl Pts',(-4.00000000000004,-6.92820323027554,-2.72936221267818E-14));
#5214=CARTESIAN_POINT('',(-8.,-4.61880215351705,-0.71453117981634));
#5215=CARTESIAN_POINT('Ctrl Pts',(-4.00000000000004,-6.92820323027554,-2.72936221267818E-14));
#5216=CARTESIAN_POINT('Ctrl Pts',(-5.8564064605665,-5.85640646054213,-2.68814782430319E-14));
#5217=CARTESIAN_POINT('Ctrl Pts',(-8.00000000003846,-4.61880215349484,-0.714531179829158));
#5218=CARTESIAN_POINT('',(-8.,-4.61880215351705,-7.68546882018366));
#5219=CARTESIAN_POINT('',(-8.,-4.61880215351704,-8.4));
#5220=CARTESIAN_POINT('',(-4.00000000000003,-6.92820323027549,-8.4));
#5221=CARTESIAN_POINT('Ctrl Pts',(-4.00000000000003,-6.92820323027555,-8.39999999999998));
#5222=CARTESIAN_POINT('Ctrl Pts',(-5.8564064605665,-5.85640646054213,-8.39999999999998));
#5223=CARTESIAN_POINT('Ctrl Pts',(-8.00000000003846,-4.61880215349483,-7.68546882017084));
#5224=CARTESIAN_POINT('Ctrl Pts',(3.83836864030079E-11,-9.23760430705625,
-7.68546882017084));
#5225=CARTESIAN_POINT('Ctrl Pts',(-2.14359353943357,-8.00000000000896,-8.39999999999997));
#5226=CARTESIAN_POINT('Ctrl Pts',(-4.00000000000003,-6.92820323027555,-8.39999999999998));
#5227=CARTESIAN_POINT('Origin',(-8.,4.61880215351699,-8.4));
#5228=CARTESIAN_POINT('',(-8.,0.,0.));
#5229=CARTESIAN_POINT('Ctrl Pts',(-8.00000000000001,-4.61880215356147,-0.714531179829163));
#5230=CARTESIAN_POINT('Ctrl Pts',(-8.00000000000001,-2.14359353946685,-3.88578058618805E-16));
#5231=CARTESIAN_POINT('Ctrl Pts',(-8.,4.40219711722286E-15,-8.80439423444572E-16));
#5232=CARTESIAN_POINT('Ctrl Pts',(-8.,4.40219711722286E-15,-8.80439423444572E-16));
#5233=CARTESIAN_POINT('Ctrl Pts',(-8.,2.14359353946683,-1.72112737696137E-15));
#5234=CARTESIAN_POINT('Ctrl Pts',(-8.00000000000001,4.61880215356141,-0.714531179829147));
#5235=CARTESIAN_POINT('',(-8.,0.,-8.4));
#5236=CARTESIAN_POINT('Ctrl Pts',(-8.,-1.49674701985577E-14,-8.4));
#5237=CARTESIAN_POINT('Ctrl Pts',(-8.,2.14359353946684,-8.4));
#5238=CARTESIAN_POINT('Ctrl Pts',(-8.,4.61880215356146,-7.68546882017084));
#5239=CARTESIAN_POINT('Ctrl Pts',(-8.,-4.61880215356146,-7.68546882017084));
#5240=CARTESIAN_POINT('Ctrl Pts',(-8.,-2.14359353946686,-8.4));
#5241=CARTESIAN_POINT('Ctrl Pts',(-8.,-1.49674701985577E-14,-8.4));
#5242=CARTESIAN_POINT('Origin',(-1.73472347597681E-15,9.23760430703403,
0.));
#5243=CARTESIAN_POINT('Origin',(0.,0.,0.));
#5244=CARTESIAN_POINT('Origin',(0.,0.,0.));
#5245=CARTESIAN_POINT('Origin',(0.,0.,0.));
#5246=CARTESIAN_POINT('Origin',(0.,0.,0.));
#5247=CARTESIAN_POINT('Origin',(0.,0.,0.));
#5248=CARTESIAN_POINT('Origin',(0.,0.,0.));
#5249=CARTESIAN_POINT('Origin',(-1.73472347597681E-15,9.23760430703403,
-8.4));
#5250=CARTESIAN_POINT('Origin',(0.,0.,-8.4));
#5251=CARTESIAN_POINT('Origin',(0.,0.,-8.4));
#5252=CARTESIAN_POINT('Origin',(0.,0.,-8.4));
#5253=CARTESIAN_POINT('Origin',(0.,0.,-8.4));
#5254=CARTESIAN_POINT('Origin',(0.,0.,-8.4));
#5255=CARTESIAN_POINT('Origin',(0.,0.,-8.4));
#5256=CARTESIAN_POINT('Origin',(0.,0.,-8.4));
#5257=CARTESIAN_POINT('Origin',(0.,0.,-8.4));
#5258=CARTESIAN_POINT('Origin',(0.,0.,-8.4));
#5259=CARTESIAN_POINT('Origin',(0.,0.,-8.4));
#5260=CARTESIAN_POINT('Origin',(0.,0.,-8.4));
#5261=CARTESIAN_POINT('Origin',(0.,0.,-8.4));
#5262=CARTESIAN_POINT('Origin',(0.,0.,0.));
#5263=CARTESIAN_POINT('Origin',(0.,0.,0.));
#5264=CARTESIAN_POINT('Origin',(0.,0.,0.));
#5265=CARTESIAN_POINT('Origin',(0.,0.,0.));
#5266=CARTESIAN_POINT('Origin',(0.,0.,0.));
#5267=CARTESIAN_POINT('Origin',(0.,0.,0.));
#5639=UNCERTAINTY_MEASURE_WITH_UNIT(LENGTH_MEASURE(0.01),#5659,
'DISTANCE_ACCURACY_VALUE',
'Maximum model space distance between geometric entities at asserted c
onnectivities');
#5645=UNCERTAINTY_MEASURE_WITH_UNIT(LENGTH_MEASURE(0.01),#5659,
'DISTANCE_ACCURACY_VALUE',
'Maximum model space distance between geometric entities at asserted c
onnectivities');
#5652=(
GEOMETRIC_REPRESENTATION_CONTEXT(3)
GLOBAL_UNCERTAINTY_ASSIGNED_CONTEXT((#5639))
GLOBAL_UNIT_ASSIGNED_CONTEXT((#5659,#5661,#5662))
REPRESENTATION_CONTEXT('','3D')
);
#5658=(
GEOMETRIC_REPRESENTATION_CONTEXT(3)
GLOBAL_UNCERTAINTY_ASSIGNED_CONTEXT((#5645))
GLOBAL_UNIT_ASSIGNED_CONTEXT((#5659,#5661,#5662))
REPRESENTATION_CONTEXT('','3D')
);
#5659=(
LENGTH_UNIT()
NAMED_UNIT(*)
SI_UNIT(.MILLI.,.METRE.)
);
#5661=(
NAMED_UNIT(*)
PLANE_ANGLE_UNIT()
SI_UNIT($,.RADIAN.)
);
#5662=(
NAMED_UNIT(*)
SI_UNIT($,.STERADIAN.)
SOLID_ANGLE_UNIT()
);
#5669=SHAPE_DEFINITION_REPRESENTATION(#5681,#5711);
#5681=PRODUCT_DEFINITION_SHAPE('',$,#5724);
#5711=SHAPE_REPRESENTATION('',(#3361),#5652);
#5717=PRODUCT_DEFINITION_CONTEXT('part definition',#5755,'design');
#5724=PRODUCT_DEFINITION('Hex Nut M10 x 1.5','Hex Nut M10 x 1.5',#5736,
#5717);
#5736=PRODUCT_DEFINITION_FORMATION('',$,#5763);
#5755=APPLICATION_CONTEXT(
'Core Data for Automotive Mechanical Design Process');
#5756=PRODUCT_CONTEXT('part definition',#5755,'mechanical');
#5763=PRODUCT('Hex Nut M10 x 1.5','Hex Nut M10 x 1.5',$,(#5756));
#5770=PRESENTATION_STYLE_ASSIGNMENT((#5775));
#5775=SURFACE_STYLE_USAGE(.BOTH.,#5780);
#5780=SURFACE_SIDE_STYLE('',(#5785));
#5785=SURFACE_STYLE_FILL_AREA(#5790);
#5790=FILL_AREA_STYLE('Opaque(31,36,43)',(#5795));
#5795=FILL_AREA_STYLE_COLOUR('Opaque(31,36,43)',#5800);
#5800=COLOUR_RGB('Opaque(31,36,43)',0.12156862745098,0.141176470588235,
0.168627450980392);
ENDSEC;
END-ISO-10303-21;
